ISO-10303-21;
HEADER;
FILE_DESCRIPTION (('STEP AP214'),
    '1' );
FILE_NAME ('o-rings series a_iso_O-ring 20x2.65-A-ISO 3601-1.step',
    '2026-09-29T11:11:29',
    ( '' ),
    ( '' ),
    'SwSTEP 2.0',
    'SolidWorks 2026',
    '' );
FILE_SCHEMA (( 'AUTOMOTIVE_DESIGN' ));
ENDSEC;

DATA;
#20=PRODUCT_DEFINITION_FORMATION_WITH_SPECIFIED_SOURCE ( 'ANY', '', #288, .NOT_KNOWN. ) ;
#77=FACE_OUTER_BOUND ( 'NONE', #632, .T. ) ;
#154=ADVANCED_FACE ( 'NONE', ( #77 ), #1363, .T. ) ;
#233=SURFACE_SIDE_STYLE ('',( #7637 ) ) ;
#288=PRODUCT ( 'o-rings series a_iso_O-ring 20x2.65-A-ISO 3601-1', 'o-rings series a_iso_O-ring 20x2.65-A-ISO 3601-1', '', ( #6267 ) ) ;
#410=( NAMED_UNIT ( * ) SI_UNIT ( $, .STERADIAN. ) SOLID_ANGLE_UNIT ( ) );
#425=PRODUCT_DEFINITION_CONTEXT ( 'detailed design', #6216, 'design' ) ;
#492=SURFACE_SIDE_STYLE ('',( #7789 ) ) ;
#501=CARTESIAN_POINT ( 'NONE',  ( 0.000000000000000000, 0.000000000000000000, 0.000000000000000000 ) ) ;
#509=AXIS2_PLACEMENT_3D ( 'NONE', #6567, #6609, #5371 ) ;
#546=TOROIDAL_SURFACE ( 'NONE', #3100, 11.32499999999999929, 1.324999999999999956 ) ;
#575=AXIS2_PLACEMENT_3D ( 'NONE', #8671, #6590, #5266 ) ;
#632=EDGE_LOOP ( 'NONE', ( #5483, #7666, #5670, #7686 ) ) ;
#716=PRESENTATION_STYLE_ASSIGNMENT (( #3549 ) ) ;
#763=( NAMED_UNIT ( * ) PLANE_ANGLE_UNIT ( ) SI_UNIT ( $, .RADIAN. ) );
#764=VERTEX_POINT ( 'NONE', #5766 ) ;
#819=DIRECTION ( 'NONE',  ( -1.224646799147353207E-16, 1.000000000000000000, 0.000000000000000000 ) ) ;
#834=EDGE_CURVE ( 'NONE', #4208, #4354, #6639, .T. ) ;
#1004=( GEOMETRIC_REPRESENTATION_CONTEXT ( 3 ) GLOBAL_UNCERTAINTY_ASSIGNED_CONTEXT ( ( #3687 ) ) GLOBAL_UNIT_ASSIGNED_CONTEXT ( ( #7291, #1426, #2761 ) ) REPRESENTATION_CONTEXT ( 'NONE', 'WORKASPACE' ) );
#1017=CARTESIAN_POINT ( 'NONE',  ( -11.32499999999999929, 0.000000000000000000, 0.000000000000000000 ) ) ;
#1078=DIRECTION ( 'NONE',  ( -1.000000000000000000, -1.224646799147352961E-16, 0.000000000000000000 ) ) ;
#1120=CARTESIAN_POINT ( 'NONE',  ( -12.65000000000000036, 0.000000000000000000, 0.000000000000000000 ) ) ;
#1202=APPLICATION_CONTEXT ( 'automotive_design' ) ;
#1256=CARTESIAN_POINT ( 'NONE',  ( 11.32499999999999929, 1.386912500034377407E-15, 0.000000000000000000 ) ) ;
#1308=TOROIDAL_SURFACE ( 'NONE', #7793, 11.32499999999999929, 1.324999999999999956 ) ;
#1342=ORIENTED_EDGE ( 'NONE', *, *, #5457, .T. ) ;
#1363=TOROIDAL_SURFACE ( 'NONE', #5298, 11.32499999999999929, 1.324999999999999956 ) ;
#1396=EDGE_CURVE ( 'NONE', #4453, #4354, #2482, .T. ) ;
#1426=( NAMED_UNIT ( * ) PLANE_ANGLE_UNIT ( ) SI_UNIT ( $, .RADIAN. ) );
#1593=COLOUR_RGB ( '', 0.72549020, 0.75294118, 0.79215686) ;
#1596=DIRECTION ( 'NONE',  ( -0.000000000000000000, -0.000000000000000000, -1.000000000000000000 ) ) ;
#1707=DIRECTION ( 'NONE',  ( 0.000000000000000000, 0.000000000000000000, 1.000000000000000000 ) ) ;
#1751=DIRECTION ( 'NONE',  ( -1.224646799147353207E-16, 1.000000000000000000, 0.000000000000000000 ) ) ;
#1767=DIRECTION ( 'NONE',  ( -0.000000000000000000, -0.000000000000000000, -1.000000000000000000 ) ) ;
#1769=ORIENTED_EDGE ( 'NONE', *, *, #2902, .T. ) ;
#1838=CIRCLE ( 'NONE', #2539, 12.65000000000000036 ) ;
#1849=DIRECTION ( 'NONE',  ( -1.000000000000000000, 0.000000000000000000, 0.000000000000000000 ) ) ;
#1892=DIRECTION ( 'NONE',  ( -1.000000000000000000, 0.000000000000000000, 0.000000000000000000 ) ) ;
#2048=CARTESIAN_POINT ( 'NONE',  ( -10.00000000000000000, 0.000000000000000000, 1.622657008870243228E-16 ) ) ;
#2140=COLOUR_RGB ( '', 0.72549020, 0.75294118, 0.79215686) ;
#2176=SHAPE_DEFINITION_REPRESENTATION ( #5009, #3450 ) ;
#2309=AXIS2_PLACEMENT_3D ( 'NONE', #1256, #819, #2944 ) ;
#2428=CARTESIAN_POINT ( 'NONE',  ( 0.000000000000000000, 0.000000000000000000, 1.622657008870242981E-16 ) ) ;
#2440=AXIS2_PLACEMENT_3D ( 'NONE', #501, #3826, #7091 ) ;
#2482=CIRCLE ( 'NONE', #8120, 10.00000000000000000 ) ;
#2539=AXIS2_PLACEMENT_3D ( 'NONE', #7911, #8572, #4474 ) ;
#2554=AXIS2_PLACEMENT_3D ( 'NONE', #7787, #1707, #3692 ) ;
#2574=EDGE_CURVE ( 'NONE', #764, #4208, #7785, .T. ) ;
#2705=ORIENTED_EDGE ( 'NONE', *, *, #8170, .F. ) ;
#2761=( NAMED_UNIT ( * ) SI_UNIT ( $, .STERADIAN. ) SOLID_ANGLE_UNIT ( ) );
#2832=UNCERTAINTY_MEASURE_WITH_UNIT (LENGTH_MEASURE( 1.000000000000000082E-05 ), #3818, 'distance_accuracy_value', 'NONE');
#2890=FACE_OUTER_BOUND ( 'NONE', #4342, .T. ) ;
#2898=EDGE_LOOP ( 'NONE', ( #7399, #7088, #4815, #7618 ) ) ;
#2902=EDGE_CURVE ( 'NONE', #764, #4453, #6795, .T. ) ;
#2944=DIRECTION ( 'NONE',  ( -1.000000000000000000, -1.224646799147352961E-16, 0.000000000000000000 ) ) ;
#3048=MANIFOLD_SOLID_BREP ( 'Sweep1', #7016 ) ;
#3100=AXIS2_PLACEMENT_3D ( 'NONE', #3419, #1596, #6270 ) ;
#3136=ORIENTED_EDGE ( 'NONE', *, *, #6699, .T. ) ;
#3205=ORIENTED_EDGE ( 'NONE', *, *, #4194, .F. ) ;
#3263=ADVANCED_FACE ( 'NONE', ( #8702 ), #1308, .T. ) ;
#3419=CARTESIAN_POINT ( 'NONE',  ( 0.000000000000000000, 0.000000000000000000, 0.000000000000000000 ) ) ;
#3423=( LENGTH_UNIT ( ) NAMED_UNIT ( * ) SI_UNIT ( .MILLI., .METRE. ) );
#3450=SHAPE_REPRESENTATION ( 'o-rings series a_iso_O-ring 20x2.65-A-ISO 3601-1', ( #2554 ), #1004 ) ;
#3549=SURFACE_STYLE_USAGE ( .BOTH. , #233 ) ;
#3685=MECHANICAL_DESIGN_GEOMETRIC_PRESENTATION_REPRESENTATION('',(#5089),#4810);
#3687=UNCERTAINTY_MEASURE_WITH_UNIT (LENGTH_MEASURE( 1.000000000000000082E-05 ), #7291, 'distance_accuracy_value', 'NONE');
#3692=DIRECTION ( 'NONE',  ( 1.000000000000000000, 0.000000000000000000, 0.000000000000000000 ) ) ;
#3818=( LENGTH_UNIT ( ) NAMED_UNIT ( * ) SI_UNIT ( .MILLI., .METRE. ) );
#3826=DIRECTION ( 'NONE',  ( -0.000000000000000000, -0.000000000000000000, -1.000000000000000000 ) ) ;
#3846=STYLED_ITEM ( 'NONE', ( #5929 ), #3048 ) ;
#3867=ADVANCED_FACE ( 'NONE', ( #2890 ), #546, .T. ) ;
#3896=CIRCLE ( 'NONE', #5291, 1.324999999999999734 ) ;
#3981=AXIS2_PLACEMENT_3D ( 'NONE', #2428, #1767, #1849 ) ;
#4123=DIRECTION ( 'NONE',  ( -1.000000000000000000, 0.000000000000000000, 0.000000000000000000 ) ) ;
#4194=EDGE_CURVE ( 'NONE', #4208, #764, #1838, .T. ) ;
#4198=FILL_AREA_STYLE ('',( #7541 ) ) ;
#4208=VERTEX_POINT ( 'NONE', #1120 ) ;
#4223=ORIENTED_EDGE ( 'NONE', *, *, #834, .F. ) ;
#4320=PRODUCT_DEFINITION ( 'UNKNOWN', '', #20, #425 ) ;
#4342=EDGE_LOOP ( 'NONE', ( #4223, #4831, #1769, #4395 ) ) ;
#4354=VERTEX_POINT ( 'NONE', #2048 ) ;
#4395=ORIENTED_EDGE ( 'NONE', *, *, #6699, .F. ) ;
#4453=VERTEX_POINT ( 'NONE', #5338 ) ;
#4474=DIRECTION ( 'NONE',  ( -1.000000000000000000, 0.000000000000000000, 0.000000000000000000 ) ) ;
#4810=( GEOMETRIC_REPRESENTATION_CONTEXT ( 3 ) GLOBAL_UNCERTAINTY_ASSIGNED_CONTEXT ( ( #5706 ) ) GLOBAL_UNIT_ASSIGNED_CONTEXT ( ( #3423, #763, #7508 ) ) REPRESENTATION_CONTEXT ( 'NONE', 'WORKASPACE' ) );
#4815=ORIENTED_EDGE ( 'NONE', *, *, #1396, .T. ) ;
#4831=ORIENTED_EDGE ( 'NONE', *, *, #4194, .T. ) ;
#4893=DIRECTION ( 'NONE',  ( -0.000000000000000000, -0.000000000000000000, -1.000000000000000000 ) ) ;
#5009=PRODUCT_DEFINITION_SHAPE ( 'NONE', 'NONE',  #4320 ) ;
#5089=STYLED_ITEM ( 'NONE', ( #716 ), #7491 ) ;
#5209=ADVANCED_FACE ( 'NONE', ( #8648 ), #8135, .T. ) ;
#5266=DIRECTION ( 'NONE',  ( 0.000000000000000000, 0.000000000000000000, -1.000000000000000000 ) ) ;
#5291=AXIS2_PLACEMENT_3D ( 'NONE', #7116, #1751, #1078 ) ;
#5298=AXIS2_PLACEMENT_3D ( 'NONE', #8206, #4893, #7570 ) ;
#5338=CARTESIAN_POINT ( 'NONE',  ( 10.00000000000000000, 1.224646799147353256E-15, 0.000000000000000000 ) ) ;
#5371=DIRECTION ( 'NONE',  ( -1.000000000000000000, 0.000000000000000000, 0.000000000000000000 ) ) ;
#5457=EDGE_CURVE ( 'NONE', #4453, #764, #3896, .T. ) ;
#5483=ORIENTED_EDGE ( 'NONE', *, *, #2902, .F. ) ;
#5670=ORIENTED_EDGE ( 'NONE', *, *, #834, .T. ) ;
#5682=MECHANICAL_DESIGN_GEOMETRIC_PRESENTATION_REPRESENTATION('',(#3846),#7224);
#5706=UNCERTAINTY_MEASURE_WITH_UNIT (LENGTH_MEASURE( 1.000000000000000082E-05 ), #3423, 'distance_accuracy_value', 'NONE');
#5766=CARTESIAN_POINT ( 'NONE',  ( 12.65000000000000036, 1.549178200921401754E-15, 0.000000000000000000 ) ) ;
#5891=( NAMED_UNIT ( * ) PLANE_ANGLE_UNIT ( ) SI_UNIT ( $, .RADIAN. ) );
#5929=PRESENTATION_STYLE_ASSIGNMENT (( #7123 ) ) ;
#6100=DIRECTION ( 'NONE',  ( -0.000000000000000000, -0.000000000000000000, -1.000000000000000000 ) ) ;
#6216=APPLICATION_CONTEXT ( 'automotive_design' ) ;
#6232=FILL_AREA_STYLE_COLOUR ( '', #2140 ) ;
#6267=PRODUCT_CONTEXT ( 'NONE', #1202, 'mechanical' ) ;
#6270=DIRECTION ( 'NONE',  ( -1.000000000000000000, 0.000000000000000000, 0.000000000000000000 ) ) ;
#6567=CARTESIAN_POINT ( 'NONE',  ( 0.000000000000000000, 0.000000000000000000, 0.000000000000000000 ) ) ;
#6590=DIRECTION ( 'NONE',  ( 0.000000000000000000, -1.000000000000000000, 0.000000000000000000 ) ) ;
#6593=DIRECTION ( 'NONE',  ( -0.000000000000000000, -0.000000000000000000, -1.000000000000000000 ) ) ;
#6609=DIRECTION ( 'NONE',  ( -0.000000000000000000, -0.000000000000000000, -1.000000000000000000 ) ) ;
#6617=CIRCLE ( 'NONE', #8033, 1.324999999999999956 ) ;
#6639=CIRCLE ( 'NONE', #575, 1.324999999999999956 ) ;
#6699=EDGE_CURVE ( 'NONE', #4354, #4453, #7782, .T. ) ;
#6795=CIRCLE ( 'NONE', #2309, 1.324999999999999734 ) ;
#6844=FILL_AREA_STYLE ('',( #6232 ) ) ;
#7016=CLOSED_SHELL ( 'NONE', ( #154, #3867, #3263, #5209 ) ) ;
#7057=DIRECTION ( 'NONE',  ( 0.000000000000000000, 0.000000000000000000, -1.000000000000000000 ) ) ;
#7088=ORIENTED_EDGE ( 'NONE', *, *, #5457, .F. ) ;
#7091=DIRECTION ( 'NONE',  ( -1.000000000000000000, 0.000000000000000000, 0.000000000000000000 ) ) ;
#7116=CARTESIAN_POINT ( 'NONE',  ( 11.32499999999999929, 1.386912500034377407E-15, 0.000000000000000000 ) ) ;
#7123=SURFACE_STYLE_USAGE ( .BOTH. , #492 ) ;
#7224=( GEOMETRIC_REPRESENTATION_CONTEXT ( 3 ) GLOBAL_UNCERTAINTY_ASSIGNED_CONTEXT ( ( #2832 ) ) GLOBAL_UNIT_ASSIGNED_CONTEXT ( ( #3818, #5891, #410 ) ) REPRESENTATION_CONTEXT ( 'NONE', 'WORKASPACE' ) );
#7291=( LENGTH_UNIT ( ) NAMED_UNIT ( * ) SI_UNIT ( .MILLI., .METRE. ) );
#7303=CARTESIAN_POINT ( 'NONE',  ( 0.000000000000000000, 0.000000000000000000, 1.622657008870242981E-16 ) ) ;
#7399=ORIENTED_EDGE ( 'NONE', *, *, #2574, .F. ) ;
#7491=ADVANCED_BREP_SHAPE_REPRESENTATION ( '', ( #3048, #2554 ), #1004 ) ;
#7508=( NAMED_UNIT ( * ) SI_UNIT ( $, .STERADIAN. ) SOLID_ANGLE_UNIT ( ) );
#7510=CARTESIAN_POINT ( 'NONE',  ( 0.000000000000000000, 0.000000000000000000, 0.000000000000000000 ) ) ;
#7541=FILL_AREA_STYLE_COLOUR ( '', #1593 ) ;
#7549=SHAPE_REPRESENTATION_RELATIONSHIP ( 'NONE' , 'NONE' ,  #3450, #7491 ) ;
#7570=DIRECTION ( 'NONE',  ( -1.000000000000000000, 0.000000000000000000, 0.000000000000000000 ) ) ;
#7583=DIRECTION ( 'NONE',  ( 0.000000000000000000, -1.000000000000000000, 0.000000000000000000 ) ) ;
#7618=ORIENTED_EDGE ( 'NONE', *, *, #8170, .T. ) ;
#7637=SURFACE_STYLE_FILL_AREA ( #6844 ) ;
#7666=ORIENTED_EDGE ( 'NONE', *, *, #2574, .T. ) ;
#7686=ORIENTED_EDGE ( 'NONE', *, *, #1396, .F. ) ;
#7782=CIRCLE ( 'NONE', #3981, 10.00000000000000000 ) ;
#7785=CIRCLE ( 'NONE', #2440, 12.65000000000000036 ) ;
#7787=CARTESIAN_POINT ( 'NONE',  ( 0.000000000000000000, 0.000000000000000000, 0.000000000000000000 ) ) ;
#7789=SURFACE_STYLE_FILL_AREA ( #4198 ) ;
#7793=AXIS2_PLACEMENT_3D ( 'NONE', #7510, #6100, #4123 ) ;
#7911=CARTESIAN_POINT ( 'NONE',  ( 0.000000000000000000, 0.000000000000000000, 0.000000000000000000 ) ) ;
#7976=EDGE_LOOP ( 'NONE', ( #3205, #2705, #3136, #1342 ) ) ;
#8033=AXIS2_PLACEMENT_3D ( 'NONE', #1017, #7583, #7057 ) ;
#8120=AXIS2_PLACEMENT_3D ( 'NONE', #7303, #6593, #1892 ) ;
#8135=TOROIDAL_SURFACE ( 'NONE', #509, 11.32499999999999929, 1.324999999999999956 ) ;
#8170=EDGE_CURVE ( 'NONE', #4354, #4208, #6617, .T. ) ;
#8206=CARTESIAN_POINT ( 'NONE',  ( 0.000000000000000000, 0.000000000000000000, 0.000000000000000000 ) ) ;
#8572=DIRECTION ( 'NONE',  ( -0.000000000000000000, -0.000000000000000000, -1.000000000000000000 ) ) ;
#8648=FACE_OUTER_BOUND ( 'NONE', #2898, .T. ) ;
#8671=CARTESIAN_POINT ( 'NONE',  ( -11.32499999999999929, 0.000000000000000000, 0.000000000000000000 ) ) ;
#8702=FACE_OUTER_BOUND ( 'NONE', #7976, .T. ) ;
ENDSEC;
END-ISO-10303-21;
